ISO-10303-21;
HEADER;
/* Generated by software containing ST-Developer
 * from STEP Tools, Inc. (www.steptools.com) 
 */

FILE_DESCRIPTION(
/* description */ ('STEP AP214'),
/* implementation_level */ '2;1');

FILE_NAME(
/* name */ 'bolt.step',
/* time_stamp */ '2026-11-14T21:09:07-08:00',
/* author */ (''),
/* organization */ (''),
/* preprocessor_version */ 'ST-DEVELOPER v20.2',
/* originating_system */ 'Autodesk Translation Framework v15.17.0.0',
/* authorisation */ '');

FILE_SCHEMA (('AUTOMOTIVE_DESIGN { 1 0 10303 214 3 1 1 }'));
ENDSEC;

DATA;
#10=MECHANICAL_DESIGN_GEOMETRIC_PRESENTATION_REPRESENTATION('',(#80),#2059);
#63=TOROIDAL_SURFACE('',#1112,15.,10.);
#66=SHAPE_REPRESENTATION_RELATIONSHIP('SRR','None',#2096,#73);
#73=ADVANCED_BREP_SHAPE_REPRESENTATION('',(#87),#2054);
#80=STYLED_ITEM('',(#2140),#87);
#87=MANIFOLD_SOLID_BREP('Body1',#977);
#109=PLANE('',#1123);
#110=PLANE('',#1124);
#111=PLANE('',#1125);
#137=FACE_BOUND('',#255,.T.);
#138=FACE_BOUND('',#258,.T.);
#146=B_SPLINE_CURVE_WITH_KNOTS('',3,(#1693,#1694,#1695,#1696,#1697,#1698,
#1699,#1700,#1701,#1702,#1703,#1704,#1705,#1706,#1707,#1708,#1709,#1710),
 .UNSPECIFIED.,.F.,.F.,(4,2,2,2,2,2,2,2,4),(0.377444585314899,0.471804471485951,
0.566164357657003,0.660526764143401,0.754889170629798,0.849251577116196,
0.943613983602594,1.03797386977365,1.1323337559447),.UNSPECIFIED.);
#147=B_SPLINE_CURVE_WITH_KNOTS('',3,(#1713,#1714,#1715,#1716,#1717,#1718,
#1719,#1720,#1721,#1722,#1723,#1724,#1725,#1726,#1727,#1728,#1729,#1730,
#1731,#1732,#1733,#1734,#1735,#1736,#1737,#1738,#1739,#1740,#1741,#1742,
#1743,#1744,#1745,#1746),.UNSPECIFIED.,.T.,.F.,(4,2,2,2,2,2,2,2,2,2,2,2,
2,2,2,2,4),(-1.5097783412596,-1.4154159347732,-1.3210535282868,-1.22669364211575,
-1.1323337559447,-1.03797386977365,-0.943613983602594,-0.849251577116196,
-0.754889170629798,-0.660526764143401,-0.566164357657003,-0.471804471485951,
-0.377444585314899,-0.283084699143847,-0.188724812972796,-0.0943624064863978,
0.),.UNSPECIFIED.);
#148=B_SPLINE_CURVE_WITH_KNOTS('',3,(#1747,#1748,#1749,#1750,#1751,#1752,
#1753,#1754,#1755,#1756,#1757,#1758,#1759,#1760,#1761,#1762,#1763,#1764,
#1765),.UNSPECIFIED.,.F.,.F.,(4,2,2,2,3,2,2,2,4),(1.1323337559447,1.22669364211575,
1.3210535282868,1.4154159347732,1.5097783412596,1.60414074774599,1.69850315423239,
1.79286304040344,1.8872229265745),.UNSPECIFIED.);
#183=FACE_OUTER_BOUND('',#251,.T.);
#184=FACE_OUTER_BOUND('',#252,.T.);
#185=FACE_OUTER_BOUND('',#253,.T.);
#186=FACE_OUTER_BOUND('',#254,.T.);
#187=FACE_OUTER_BOUND('',#256,.T.);
#188=FACE_OUTER_BOUND('',#257,.T.);
#189=FACE_OUTER_BOUND('',#259,.T.);
#251=EDGE_LOOP('',(#781,#782,#783,#784,#785));
#252=EDGE_LOOP('',(#786,#787,#788,#789,#790));
#253=EDGE_LOOP('',(#791,#792,#793,#794,#795));
#254=EDGE_LOOP('',(#796,#797,#798,#799,#800,#801,#802,#803));
#255=EDGE_LOOP('',(#804));
#256=EDGE_LOOP('',(#805));
#257=EDGE_LOOP('',(#806));
#258=EDGE_LOOP('',(#807));
#259=EDGE_LOOP('',(#808));
#327=LINE('',#1712,#392);
#328=LINE('',#1769,#393);
#329=LINE('',#1773,#394);
#330=LINE('',#1775,#395);
#392=VECTOR('',#1335,2.5);
#393=VECTOR('',#1340,25.);
#394=VECTOR('',#1345,15.);
#395=VECTOR('',#1346,15.);
#439=CIRCLE('',#1113,15.);
#440=CIRCLE('',#1114,10.);
#441=CIRCLE('',#1115,25.);
#442=CIRCLE('',#1116,25.);
#443=CIRCLE('',#1119,25.);
#444=CIRCLE('',#1121,15.);
#445=CIRCLE('',#1122,15.);
#501=VERTEX_POINT('',#1683);
#502=VERTEX_POINT('',#1685);
#503=VERTEX_POINT('',#1687);
#504=VERTEX_POINT('',#1691);
#505=VERTEX_POINT('',#1692);
#506=VERTEX_POINT('',#1711);
#507=VERTEX_POINT('',#1767);
#508=VERTEX_POINT('',#1771);
#509=VERTEX_POINT('',#1774);
#601=EDGE_CURVE('',#501,#501,#439,.T.);
#602=EDGE_CURVE('',#501,#502,#440,.T.);
#603=EDGE_CURVE('',#503,#502,#441,.T.);
#604=EDGE_CURVE('',#502,#503,#442,.T.);
#605=EDGE_CURVE('',#504,#505,#146,.T.);
#606=EDGE_CURVE('',#504,#506,#327,.T.);
#607=EDGE_CURVE('',#506,#506,#147,.T.);
#608=EDGE_CURVE('',#505,#504,#148,.T.);
#609=EDGE_CURVE('',#507,#507,#443,.T.);
#610=EDGE_CURVE('',#507,#503,#328,.T.);
#611=EDGE_CURVE('',#508,#508,#444,.T.);
#612=EDGE_CURVE('',#508,#504,#329,.T.);
#613=EDGE_CURVE('',#505,#509,#330,.T.);
#614=EDGE_CURVE('',#509,#509,#445,.T.);
#781=ORIENTED_EDGE('',*,*,#601,.F.);
#782=ORIENTED_EDGE('',*,*,#602,.T.);
#783=ORIENTED_EDGE('',*,*,#603,.F.);
#784=ORIENTED_EDGE('',*,*,#604,.F.);
#785=ORIENTED_EDGE('',*,*,#602,.F.);
#786=ORIENTED_EDGE('',*,*,#605,.F.);
#787=ORIENTED_EDGE('',*,*,#606,.T.);
#788=ORIENTED_EDGE('',*,*,#607,.F.);
#789=ORIENTED_EDGE('',*,*,#606,.F.);
#790=ORIENTED_EDGE('',*,*,#608,.F.);
#791=ORIENTED_EDGE('',*,*,#609,.T.);
#792=ORIENTED_EDGE('',*,*,#610,.T.);
#793=ORIENTED_EDGE('',*,*,#603,.T.);
#794=ORIENTED_EDGE('',*,*,#604,.T.);
#795=ORIENTED_EDGE('',*,*,#610,.F.);
#796=ORIENTED_EDGE('',*,*,#611,.F.);
#797=ORIENTED_EDGE('',*,*,#612,.T.);
#798=ORIENTED_EDGE('',*,*,#605,.T.);
#799=ORIENTED_EDGE('',*,*,#613,.T.);
#800=ORIENTED_EDGE('',*,*,#614,.T.);
#801=ORIENTED_EDGE('',*,*,#613,.F.);
#802=ORIENTED_EDGE('',*,*,#608,.T.);
#803=ORIENTED_EDGE('',*,*,#612,.F.);
#804=ORIENTED_EDGE('',*,*,#607,.T.);
#805=ORIENTED_EDGE('',*,*,#601,.T.);
#806=ORIENTED_EDGE('',*,*,#609,.F.);
#807=ORIENTED_EDGE('',*,*,#611,.T.);
#808=ORIENTED_EDGE('',*,*,#614,.F.);
#907=CYLINDRICAL_SURFACE('',#1117,2.5);
#908=CYLINDRICAL_SURFACE('',#1118,25.);
#909=CYLINDRICAL_SURFACE('',#1120,15.);
#946=ADVANCED_FACE('',(#183),#63,.T.);
#947=ADVANCED_FACE('',(#184),#907,.F.);
#948=ADVANCED_FACE('',(#185),#908,.T.);
#949=ADVANCED_FACE('',(#186,#137),#909,.T.);
#950=ADVANCED_FACE('',(#187),#109,.T.);
#951=ADVANCED_FACE('',(#188,#138),#110,.F.);
#952=ADVANCED_FACE('',(#189),#111,.F.);
#977=CLOSED_SHELL('',(#946,#947,#948,#949,#950,#951,#952));
#1111=AXIS2_PLACEMENT_3D('',#1681,#1321,#1322);
#1112=AXIS2_PLACEMENT_3D('',#1682,#1323,#1324);
#1113=AXIS2_PLACEMENT_3D('',#1684,#1325,#1326);
#1114=AXIS2_PLACEMENT_3D('',#1686,#1327,#1328);
#1115=AXIS2_PLACEMENT_3D('',#1688,#1329,#1330);
#1116=AXIS2_PLACEMENT_3D('',#1689,#1331,#1332);
#1117=AXIS2_PLACEMENT_3D('',#1690,#1333,#1334);
#1118=AXIS2_PLACEMENT_3D('',#1766,#1336,#1337);
#1119=AXIS2_PLACEMENT_3D('',#1768,#1338,#1339);
#1120=AXIS2_PLACEMENT_3D('',#1770,#1341,#1342);
#1121=AXIS2_PLACEMENT_3D('',#1772,#1343,#1344);
#1122=AXIS2_PLACEMENT_3D('',#1776,#1347,#1348);
#1123=AXIS2_PLACEMENT_3D('',#1777,#1349,#1350);
#1124=AXIS2_PLACEMENT_3D('',#1778,#1351,#1352);
#1125=AXIS2_PLACEMENT_3D('',#1779,#1353,#1354);
#1321=DIRECTION('axis',(0.,0.,1.));
#1322=DIRECTION('refdir',(1.,0.,0.));
#1323=DIRECTION('center_axis',(1.,4.14398494273913E-29,6.31088724176809E-30));
#1324=DIRECTION('ref_axis',(0.,-1.7347234759767E-18,-1.));
#1325=DIRECTION('center_axis',(1.,4.14398494273913E-29,6.31088724176809E-30));
#1326=DIRECTION('ref_axis',(6.31088724176809E-30,-1.7347234759767E-18,-1.));
#1327=DIRECTION('center_axis',(4.14398494273913E-29,-1.,-1.20729956438759E-16));
#1328=DIRECTION('ref_axis',(0.,-1.20729956438759E-16,1.));
#1329=DIRECTION('center_axis',(-1.,-4.14398494273913E-29,-6.31088724176809E-30));
#1330=DIRECTION('ref_axis',(6.31088724176809E-30,-1.7347234759767E-18,-1.));
#1331=DIRECTION('center_axis',(-1.,-4.14398494273913E-29,-6.31088724176809E-30));
#1332=DIRECTION('ref_axis',(6.31088724176809E-30,-1.7347234759767E-18,-1.));
#1333=DIRECTION('center_axis',(-6.50810246807336E-30,-1.7347234759767E-18,
-1.));
#1334=DIRECTION('ref_axis',(-1.,-4.14398494273912E-29,6.50810246807336E-30));
#1335=DIRECTION('',(-6.50810246807336E-30,-1.7347234759767E-18,-1.));
#1336=DIRECTION('center_axis',(-1.,-4.14398494273913E-29,-6.31088724176809E-30));
#1337=DIRECTION('ref_axis',(-6.31088724176809E-30,1.7347234759767E-18,1.));
#1338=DIRECTION('center_axis',(1.,4.14398494273913E-29,6.31088724176809E-30));
#1339=DIRECTION('ref_axis',(6.31088724176809E-30,-1.7347234759767E-18,-1.));
#1340=DIRECTION('',(1.,4.14398494273913E-29,6.31088724176809E-30));
#1341=DIRECTION('center_axis',(1.,4.14398494273913E-29,6.31088724176809E-30));
#1342=DIRECTION('ref_axis',(6.31088724176809E-30,-1.7347234759767E-18,-1.));
#1343=DIRECTION('center_axis',(1.,4.14398494273913E-29,6.31088724176809E-30));
#1344=DIRECTION('ref_axis',(6.31088724176809E-30,-1.7347234759767E-18,-1.));
#1345=DIRECTION('',(-1.,-4.14398494273913E-29,-6.31088724176809E-30));
#1346=DIRECTION('',(-1.,-4.14398494273913E-29,-6.31088724176809E-30));
#1347=DIRECTION('center_axis',(1.,4.14398494273913E-29,6.31088724176809E-30));
#1348=DIRECTION('ref_axis',(6.31088724176809E-30,-1.7347234759767E-18,-1.));
#1349=DIRECTION('center_axis',(1.,4.14398494273913E-29,-6.50810246807336E-30));
#1350=DIRECTION('ref_axis',(-6.50810246807336E-30,-1.7347234759767E-18,
-1.));
#1351=DIRECTION('center_axis',(1.,4.14398494273913E-29,-6.50810246807336E-30));
#1352=DIRECTION('ref_axis',(-6.50810246807336E-30,-1.7347234759767E-18,
-1.));
#1353=DIRECTION('center_axis',(1.,4.14398494273913E-29,-6.50810246807336E-30));
#1354=DIRECTION('ref_axis',(-6.50810246807336E-30,-1.7347234759767E-18,
-1.));
#1681=CARTESIAN_POINT('',(0.,0.,0.));
#1682=CARTESIAN_POINT('Origin',(2.5,0.,0.));
#1683=CARTESIAN_POINT('',(12.5,-1.81094934658102E-15,15.0000000000004));
#1684=CARTESIAN_POINT('Origin',(12.5,0.,4.44089209850063E-13));
#1685=CARTESIAN_POINT('',(2.5,-3.01824891096896E-15,25.));
#1686=CARTESIAN_POINT('Origin',(2.5,-1.81094934658138E-15,15.));
#1687=CARTESIAN_POINT('',(2.5,3.01824891096855E-15,-25.));
#1688=CARTESIAN_POINT('Origin',(2.5,0.,0.));
#1689=CARTESIAN_POINT('Origin',(2.5,0.,0.));
#1690=CARTESIAN_POINT('Origin',(-166.25,0.,172.5));
#1691=CARTESIAN_POINT('',(-163.75,1.86299093907171E-15,15.000000000004));
#1692=CARTESIAN_POINT('',(-168.75,-9.74863612329683E-16,15.000000000004));
#1693=CARTESIAN_POINT('Ctrl Pts',(-163.75,-1.38777878078145E-16,15.000000000004));
#1694=CARTESIAN_POINT('Ctrl Pts',(-163.75,-0.314532953903506,15.000000000004));
#1695=CARTESIAN_POINT('Ctrl Pts',(-163.8129794775,-0.649633350162397,14.9891013758676));
#1696=CARTESIAN_POINT('Ctrl Pts',(-164.068297410941,-1.26541151060516,14.9497129490472));
#1697=CARTESIAN_POINT('Ctrl Pts',(-164.260603678422,-1.54613758435443,14.9217716767288));
#1698=CARTESIAN_POINT('Ctrl Pts',(-164.703868335279,-1.98940224121134,14.8691658402804));
#1699=CARTESIAN_POINT('Ctrl Pts',(-164.984591867622,-2.18170386550857,14.8410532029514));
#1700=CARTESIAN_POINT('Ctrl Pts',(-165.600361297578,-2.43701842756375,14.8012713411856));
#1701=CARTESIAN_POINT('Ctrl Pts',(-165.935458645045,-2.5,14.790199457753));
#1702=CARTESIAN_POINT('Ctrl Pts',(-166.564541354955,-2.5,14.790199457753));
#1703=CARTESIAN_POINT('Ctrl Pts',(-166.899638702422,-2.43701842756377,14.8012713411856));
#1704=CARTESIAN_POINT('Ctrl Pts',(-167.515408132377,-2.1817038655086,14.8410532029514));
#1705=CARTESIAN_POINT('Ctrl Pts',(-167.796131664721,-1.98940224121134,14.8691658402804));
#1706=CARTESIAN_POINT('Ctrl Pts',(-168.239396321578,-1.54613758435443,14.9217716767288));
#1707=CARTESIAN_POINT('Ctrl Pts',(-168.431702589059,-1.26541151060517,14.9497129490472));
#1708=CARTESIAN_POINT('Ctrl Pts',(-168.6870205225,-0.649633350162398,14.9891013758676));
#1709=CARTESIAN_POINT('Ctrl Pts',(-168.75,-0.314532953903508,15.000000000004));
#1710=CARTESIAN_POINT('Ctrl Pts',(-168.75,-1.17961196366423E-15,15.000000000004));
#1711=CARTESIAN_POINT('',(-163.75,-2.60207403499523E-17,-14.999999999996));
#1712=CARTESIAN_POINT('',(-163.75,-3.06161699786735E-16,172.5));
#1713=CARTESIAN_POINT('Ctrl Pts',(-166.25,2.5,-14.790199457745));
#1714=CARTESIAN_POINT('Ctrl Pts',(-166.564541354955,2.5,-14.790199457745));
#1715=CARTESIAN_POINT('Ctrl Pts',(-166.899638702422,2.43701842756377,-14.8012713411776));
#1716=CARTESIAN_POINT('Ctrl Pts',(-167.515408132377,2.1817038655086,-14.8410532029434));
#1717=CARTESIAN_POINT('Ctrl Pts',(-167.796131664721,1.98940224121134,-14.8691658402724));
#1718=CARTESIAN_POINT('Ctrl Pts',(-168.239396321578,1.54613758435443,-14.9217716767208));
#1719=CARTESIAN_POINT('Ctrl Pts',(-168.431702589059,1.26541151060516,-14.9497129490392));
#1720=CARTESIAN_POINT('Ctrl Pts',(-168.6870205225,0.649633350162396,-14.9891013758596));
#1721=CARTESIAN_POINT('Ctrl Pts',(-168.75,0.314532953903506,-14.999999999996));
#1722=CARTESIAN_POINT('Ctrl Pts',(-168.75,-0.314532953903507,-14.999999999996));
#1723=CARTESIAN_POINT('Ctrl Pts',(-168.6870205225,-0.649633350162412,-14.9891013758596));
#1724=CARTESIAN_POINT('Ctrl Pts',(-168.431702589059,-1.26541151060518,-14.9497129490392));
#1725=CARTESIAN_POINT('Ctrl Pts',(-168.239396321578,-1.54613758435443,-14.9217716767208));
#1726=CARTESIAN_POINT('Ctrl Pts',(-167.796131664721,-1.98940224121134,-14.8691658402724));
#1727=CARTESIAN_POINT('Ctrl Pts',(-167.515408132377,-2.18170386550861,-14.8410532029434));
#1728=CARTESIAN_POINT('Ctrl Pts',(-166.899638702422,-2.43701842756378,-14.8012713411776));
#1729=CARTESIAN_POINT('Ctrl Pts',(-166.564541354955,-2.5,-14.790199457745));
#1730=CARTESIAN_POINT('Ctrl Pts',(-165.935458645045,-2.5,-14.790199457745));
#1731=CARTESIAN_POINT('Ctrl Pts',(-165.600361297578,-2.43701842756375,-14.8012713411776));
#1732=CARTESIAN_POINT('Ctrl Pts',(-164.984591867622,-2.18170386550857,-14.8410532029434));
#1733=CARTESIAN_POINT('Ctrl Pts',(-164.703868335279,-1.98940224121134,-14.8691658402724));
#1734=CARTESIAN_POINT('Ctrl Pts',(-164.260603678422,-1.54613758435443,-14.9217716767208));
#1735=CARTESIAN_POINT('Ctrl Pts',(-164.068297410941,-1.26541151060517,-14.9497129490392));
#1736=CARTESIAN_POINT('Ctrl Pts',(-163.8129794775,-0.649633350162397,-14.9891013758596));
#1737=CARTESIAN_POINT('Ctrl Pts',(-163.75,-0.314532953903507,-14.999999999996));
#1738=CARTESIAN_POINT('Ctrl Pts',(-163.75,0.314532953903505,-14.999999999996));
#1739=CARTESIAN_POINT('Ctrl Pts',(-163.8129794775,0.649633350162396,-14.9891013758596));
#1740=CARTESIAN_POINT('Ctrl Pts',(-164.068297410941,1.26541151060516,-14.9497129490392));
#1741=CARTESIAN_POINT('Ctrl Pts',(-164.260603678422,1.54613758435443,-14.9217716767208));
#1742=CARTESIAN_POINT('Ctrl Pts',(-164.703868335279,1.98940224121134,-14.8691658402724));
#1743=CARTESIAN_POINT('Ctrl Pts',(-164.984591867623,2.1817038655086,-14.8410532029434));
#1744=CARTESIAN_POINT('Ctrl Pts',(-165.600361297578,2.43701842756377,-14.8012713411776));
#1745=CARTESIAN_POINT('Ctrl Pts',(-165.935458645045,2.5,-14.790199457745));
#1746=CARTESIAN_POINT('Ctrl Pts',(-166.25,2.5,-14.790199457745));
#1747=CARTESIAN_POINT('Ctrl Pts',(-168.75,-6.93889390390723E-17,15.000000000004));
#1748=CARTESIAN_POINT('Ctrl Pts',(-168.75,0.314532953903506,15.000000000004));
#1749=CARTESIAN_POINT('Ctrl Pts',(-168.6870205225,0.649633350162395,14.9891013758676));
#1750=CARTESIAN_POINT('Ctrl Pts',(-168.431702589059,1.26541151060516,14.9497129490472));
#1751=CARTESIAN_POINT('Ctrl Pts',(-168.239396321578,1.54613758435443,14.9217716767288));
#1752=CARTESIAN_POINT('Ctrl Pts',(-167.796131664721,1.98940224121134,14.8691658402804));
#1753=CARTESIAN_POINT('Ctrl Pts',(-167.515408132377,2.1817038655086,14.8410532029514));
#1754=CARTESIAN_POINT('Ctrl Pts',(-166.899638702422,2.43701842756377,14.8012713411856));
#1755=CARTESIAN_POINT('Ctrl Pts',(-166.564541354955,2.5,14.790199457753));
#1756=CARTESIAN_POINT('Ctrl Pts',(-166.25,2.5,14.790199457753));
#1757=CARTESIAN_POINT('Ctrl Pts',(-165.935458645045,2.5,14.790199457753));
#1758=CARTESIAN_POINT('Ctrl Pts',(-165.600361297578,2.43701842756377,14.8012713411856));
#1759=CARTESIAN_POINT('Ctrl Pts',(-164.984591867623,2.1817038655086,14.8410532029514));
#1760=CARTESIAN_POINT('Ctrl Pts',(-164.703868335279,1.98940224121134,14.8691658402804));
#1761=CARTESIAN_POINT('Ctrl Pts',(-164.260603678422,1.54613758435443,14.9217716767288));
#1762=CARTESIAN_POINT('Ctrl Pts',(-164.068297410941,1.26541151060516,14.9497129490472));
#1763=CARTESIAN_POINT('Ctrl Pts',(-163.8129794775,0.649633350162396,14.9891013758676));
#1764=CARTESIAN_POINT('Ctrl Pts',(-163.75,0.314532953903509,15.000000000004));
#1765=CARTESIAN_POINT('Ctrl Pts',(-163.75,2.91433543964104E-15,15.000000000004));
#1766=CARTESIAN_POINT('Origin',(12.5,0.,4.44089209850063E-13));
#1767=CARTESIAN_POINT('',(0.,-3.10498508476831E-15,-24.9999999999995));
#1768=CARTESIAN_POINT('Origin',(0.,0.,0.));
#1769=CARTESIAN_POINT('',(12.5,-3.1049850847678E-15,-24.9999999999995));
#1770=CARTESIAN_POINT('Origin',(-172.5,0.,3.99680288865056E-12));
#1771=CARTESIAN_POINT('',(0.,-1.81094934657423E-15,15.000000000004));
#1772=CARTESIAN_POINT('Origin',(0.,0.,0.));
#1773=CARTESIAN_POINT('',(-172.5,-1.81094934658138E-15,15.000000000004));
#1774=CARTESIAN_POINT('',(-172.5,-1.81094934658138E-15,15.000000000004));
#1775=CARTESIAN_POINT('',(-172.5,-1.81094934658138E-15,15.000000000004));
#1776=CARTESIAN_POINT('Origin',(-172.5,0.,3.99680288865056E-12));
#1777=CARTESIAN_POINT('Origin',(12.5,0.,4.44089209850063E-13));
#1778=CARTESIAN_POINT('Origin',(0.,0.,0.));
#1779=CARTESIAN_POINT('Origin',(-172.5,0.,3.99680288865056E-12));
#2045=UNCERTAINTY_MEASURE_WITH_UNIT(LENGTH_MEASURE(0.01),#2060,
'DISTANCE_ACCURACY_VALUE',
'Maximum model space distance between geometric entities at asserted c
onnectivities');
#2050=UNCERTAINTY_MEASURE_WITH_UNIT(LENGTH_MEASURE(0.01),#2060,
'DISTANCE_ACCURACY_VALUE',
'Maximum model space distance between geometric entities at asserted c
onnectivities');
#2054=(
GEOMETRIC_REPRESENTATION_CONTEXT(3)
GLOBAL_UNCERTAINTY_ASSIGNED_CONTEXT((#2045))
GLOBAL_UNIT_ASSIGNED_CONTEXT((#2060,#2062,#2063))
REPRESENTATION_CONTEXT('','3D')
);
#2059=(
GEOMETRIC_REPRESENTATION_CONTEXT(3)
GLOBAL_UNCERTAINTY_ASSIGNED_CONTEXT((#2050))
GLOBAL_UNIT_ASSIGNED_CONTEXT((#2060,#2062,#2063))
REPRESENTATION_CONTEXT('','3D')
);
#2060=(
LENGTH_UNIT()
NAMED_UNIT(*)
SI_UNIT(.MILLI.,.METRE.)
);
#2062=(
NAMED_UNIT(*)
PLANE_ANGLE_UNIT()
SI_UNIT($,.RADIAN.)
);
#2063=(
NAMED_UNIT(*)
SI_UNIT($,.STERADIAN.)
SOLID_ANGLE_UNIT()
);
#2067=SHAPE_DEFINITION_REPRESENTATION(#2075,#2096);
#2075=PRODUCT_DEFINITION_SHAPE('',$,#2105);
#2096=SHAPE_REPRESENTATION('',(#1111),#2054);
#2101=PRODUCT_DEFINITION_CONTEXT('part definition',#2127,'design');
#2105=PRODUCT_DEFINITION('bolt','bolt',#2113,#2101);
#2113=PRODUCT_DEFINITION_FORMATION('',$,#2132);
#2127=APPLICATION_CONTEXT(
'Core Data for Automotive Mechanical Design Process');
#2128=PRODUCT_CONTEXT('part definition',#2127,'mechanical');
#2132=PRODUCT('bolt','bolt',$,(#2128));
#2140=PRESENTATION_STYLE_ASSIGNMENT((#2146));
#2146=SURFACE_STYLE_USAGE(.BOTH.,#2152);
#2152=SURFACE_SIDE_STYLE('',(#2158));
#2158=SURFACE_STYLE_FILL_AREA(#2164);
#2164=FILL_AREA_STYLE('Opaque(31,36,43)',(#2170));
#2170=FILL_AREA_STYLE_COLOUR('Opaque(31,36,43)',#2176);
#2176=COLOUR_RGB('Opaque(31,36,43)',0.12156862745098,0.141176470588235,
0.168627450980392);
ENDSEC;
END-ISO-10303-21;
